ISO-10303-21;
HEADER;
/* Generated by software containing ST-Developer
 * from STEP Tools, Inc. (www.steptools.com) 
 */

FILE_DESCRIPTION(
/* description */ ('PAT-091'),
/* implementation_level */ '2;1');

FILE_NAME(
/* name */ 'Lower screw support.step',
/* time_stamp */ '2026-10-27T15:34:44-07:00',
/* author */ (''),
/* organization */ (''),
/* preprocessor_version */ 'ST-DEVELOPER v20.2',
/* originating_system */ 'Autodesk Translation Framework v15.17.0.0',
/* authorisation */ '');

FILE_SCHEMA (('AUTOMOTIVE_DESIGN { 1 0 10303 214 3 1 1 }'));
ENDSEC;

DATA;
#10=MECHANICAL_DESIGN_GEOMETRIC_PRESENTATION_REPRESENTATION('',(#977),#25100);
#757=SHAPE_REPRESENTATION_RELATIONSHIP('SRR','None',#25518,#867);
#867=ADVANCED_BREP_SHAPE_REPRESENTATION('',(#1101),#24988);
#977=STYLED_ITEM('',(#26198),#1101);
#1101=MANIFOLD_SOLID_BREP('Body1',#13254);
#1277=FACE_BOUND('',#3021,.T.);
#1278=FACE_BOUND('',#3022,.T.);
#1279=FACE_BOUND('',#3024,.T.);
#1280=FACE_BOUND('',#3025,.T.);
#1281=FACE_BOUND('',#3030,.T.);
#1282=FACE_BOUND('',#3031,.T.);
#1283=FACE_BOUND('',#3032,.T.);
#1284=FACE_BOUND('',#3033,.T.);
#1285=FACE_BOUND('',#3034,.T.);
#1286=FACE_BOUND('',#3035,.T.);
#1287=FACE_BOUND('',#3036,.T.);
#1288=FACE_BOUND('',#3040,.T.);
#1289=FACE_BOUND('',#3041,.T.);
#1290=FACE_BOUND('',#3042,.T.);
#1291=FACE_BOUND('',#3043,.T.);
#1292=FACE_BOUND('',#3044,.T.);
#1293=FACE_BOUND('',#3045,.T.);
#1294=FACE_BOUND('',#3046,.T.);
#1295=FACE_BOUND('',#3050,.T.);
#1296=FACE_BOUND('',#3051,.T.);
#1297=FACE_BOUND('',#3052,.T.);
#1298=FACE_BOUND('',#3053,.T.);
#1674=PLANE('',#14757);
#1675=PLANE('',#14758);
#1676=PLANE('',#14759);
#1677=PLANE('',#14760);
#1678=PLANE('',#14761);
#1679=PLANE('',#14762);
#1680=PLANE('',#14769);
#1681=PLANE('',#14770);
#1682=PLANE('',#14771);
#1683=PLANE('',#14772);
#2131=FACE_OUTER_BOUND('',#3011,.T.);
#2132=FACE_OUTER_BOUND('',#3012,.T.);
#2133=FACE_OUTER_BOUND('',#3013,.T.);
#2134=FACE_OUTER_BOUND('',#3014,.T.);
#2135=FACE_OUTER_BOUND('',#3015,.T.);
#2136=FACE_OUTER_BOUND('',#3016,.T.);
#2137=FACE_OUTER_BOUND('',#3017,.T.);
#2138=FACE_OUTER_BOUND('',#3018,.T.);
#2139=FACE_OUTER_BOUND('',#3019,.T.);
#2140=FACE_OUTER_BOUND('',#3020,.T.);
#2141=FACE_OUTER_BOUND('',#3023,.T.);
#2142=FACE_OUTER_BOUND('',#3026,.T.);
#2143=FACE_OUTER_BOUND('',#3027,.T.);
#2144=FACE_OUTER_BOUND('',#3028,.T.);
#2145=FACE_OUTER_BOUND('',#3029,.T.);
#2146=FACE_OUTER_BOUND('',#3037,.T.);
#2147=FACE_OUTER_BOUND('',#3038,.T.);
#2148=FACE_OUTER_BOUND('',#3039,.T.);
#2149=FACE_OUTER_BOUND('',#3047,.T.);
#2150=FACE_OUTER_BOUND('',#3048,.T.);
#2151=FACE_OUTER_BOUND('',#3049,.T.);
#3011=EDGE_LOOP('',(#9296,#9297,#9298,#9299));
#3012=EDGE_LOOP('',(#9300,#9301,#9302,#9303));
#3013=EDGE_LOOP('',(#9304,#9305,#9306,#9307));
#3014=EDGE_LOOP('',(#9308,#9309,#9310,#9311));
#3015=EDGE_LOOP('',(#9312,#9313,#9314,#9315));
#3016=EDGE_LOOP('',(#9316,#9317,#9318,#9319));
#3017=EDGE_LOOP('',(#9320,#9321,#9322,#9323));
#3018=EDGE_LOOP('',(#9324,#9325,#9326,#9327));
#3019=EDGE_LOOP('',(#9328,#9329,#9330,#9331));
#3020=EDGE_LOOP('',(#9332,#9333,#9334,#9335));
#3021=EDGE_LOOP('',(#9336));
#3022=EDGE_LOOP('',(#9337));
#3023=EDGE_LOOP('',(#9338,#9339,#9340,#9341));
#3024=EDGE_LOOP('',(#9342));
#3025=EDGE_LOOP('',(#9343));
#3026=EDGE_LOOP('',(#9344,#9345,#9346,#9347));
#3027=EDGE_LOOP('',(#9348,#9349,#9350,#9351));
#3028=EDGE_LOOP('',(#9352,#9353,#9354,#9355,#9356,#9357,#9358,#9359));
#3029=EDGE_LOOP('',(#9360,#9361,#9362,#9363));
#3030=EDGE_LOOP('',(#9364));
#3031=EDGE_LOOP('',(#9365));
#3032=EDGE_LOOP('',(#9366));
#3033=EDGE_LOOP('',(#9367));
#3034=EDGE_LOOP('',(#9368));
#3035=EDGE_LOOP('',(#9369));
#3036=EDGE_LOOP('',(#9370));
#3037=EDGE_LOOP('',(#9371,#9372,#9373,#9374));
#3038=EDGE_LOOP('',(#9375,#9376,#9377,#9378));
#3039=EDGE_LOOP('',(#9379,#9380,#9381,#9382));
#3040=EDGE_LOOP('',(#9383));
#3041=EDGE_LOOP('',(#9384));
#3042=EDGE_LOOP('',(#9385));
#3043=EDGE_LOOP('',(#9386));
#3044=EDGE_LOOP('',(#9387));
#3045=EDGE_LOOP('',(#9388));
#3046=EDGE_LOOP('',(#9389));
#3047=EDGE_LOOP('',(#9390,#9391,#9392,#9393,#9394,#9395,#9396,#9397));
#3048=EDGE_LOOP('',(#9398,#9399,#9400,#9401));
#3049=EDGE_LOOP('',(#9402,#9403,#9404,#9405));
#3050=EDGE_LOOP('',(#9406));
#3051=EDGE_LOOP('',(#9407));
#3052=EDGE_LOOP('',(#9408));
#3053=EDGE_LOOP('',(#9409));
#4218=LINE('',#21325,#4958);
#4219=LINE('',#21331,#4959);
#4220=LINE('',#21337,#4960);
#4221=LINE('',#21343,#4961);
#4222=LINE('',#21349,#4962);
#4223=LINE('',#21355,#4963);
#4224=LINE('',#21361,#4964);
#4225=LINE('',#21367,#4965);
#4226=LINE('',#21373,#4966);
#4227=LINE('',#21378,#4967);
#4228=LINE('',#21380,#4968);
#4229=LINE('',#21382,#4969);
#4230=LINE('',#21383,#4970);
#4231=LINE('',#21387,#4971);
#4232=LINE('',#21389,#4972);
#4233=LINE('',#21391,#4973);
#4234=LINE('',#21392,#4974);
#4235=LINE('',#21396,#4975);
#4236=LINE('',#21397,#4976);
#4237=LINE('',#21398,#4977);
#4238=LINE('',#21402,#4978);
#4239=LINE('',#21403,#4979);
#4240=LINE('',#21404,#4980);
#4241=LINE('',#21407,#4981);
#4242=LINE('',#21409,#4982);
#4243=LINE('',#21410,#4983);
#4244=LINE('',#21411,#4984);
#4245=LINE('',#21414,#4985);
#4246=LINE('',#21415,#4986);
#4247=LINE('',#21422,#4987);
#4248=LINE('',#21426,#4988);
#4249=LINE('',#21430,#4989);
#4250=LINE('',#21431,#4990);
#4251=LINE('',#21433,#4991);
#4252=LINE('',#21434,#4992);
#4958=VECTOR('',#16856,0.165);
#4959=VECTOR('',#16863,0.165);
#4960=VECTOR('',#16870,0.165);
#4961=VECTOR('',#16877,0.165);
#4962=VECTOR('',#16884,1.6);
#4963=VECTOR('',#16891,0.274999999999999);
#4964=VECTOR('',#16898,0.274999999999999);
#4965=VECTOR('',#16905,0.274999999999999);
#4966=VECTOR('',#16912,0.274999999999999);
#4967=VECTOR('',#16917,1.);
#4968=VECTOR('',#16918,1.);
#4969=VECTOR('',#16919,1.);
#4970=VECTOR('',#16920,1.);
#4971=VECTOR('',#16923,1.);
#4972=VECTOR('',#16924,1.);
#4973=VECTOR('',#16925,1.);
#4974=VECTOR('',#16926,1.);
#4975=VECTOR('',#16929,1.);
#4976=VECTOR('',#16930,1.);
#4977=VECTOR('',#16931,1.);
#4978=VECTOR('',#16934,1.);
#4979=VECTOR('',#16935,1.);
#4980=VECTOR('',#16936,1.);
#4981=VECTOR('',#16939,1.);
#4982=VECTOR('',#16940,1.);
#4983=VECTOR('',#16941,1.);
#4984=VECTOR('',#16942,1.);
#4985=VECTOR('',#16945,1.);
#4986=VECTOR('',#16946,1.);
#4987=VECTOR('',#16953,0.605);
#4988=VECTOR('',#16958,0.605);
#4989=VECTOR('',#16963,1.);
#4990=VECTOR('',#16964,1.);
#4991=VECTOR('',#16967,1.);
#4992=VECTOR('',#16968,1.);
#5672=CIRCLE('',#14731,0.165);
#5673=CIRCLE('',#14732,0.165);
#5674=CIRCLE('',#14734,0.165);
#5675=CIRCLE('',#14735,0.165);
#5676=CIRCLE('',#14737,0.165);
#5677=CIRCLE('',#14738,0.165);
#5678=CIRCLE('',#14740,0.165);
#5679=CIRCLE('',#14741,0.165);
#5680=CIRCLE('',#14743,1.6);
#5681=CIRCLE('',#14744,1.6);
#5682=CIRCLE('',#14746,0.274999999999999);
#5683=CIRCLE('',#14747,0.274999999999999);
#5684=CIRCLE('',#14749,0.274999999999999);
#5685=CIRCLE('',#14750,0.274999999999999);
#5686=CIRCLE('',#14752,0.274999999999999);
#5687=CIRCLE('',#14753,0.274999999999999);
#5688=CIRCLE('',#14755,0.274999999999999);
#5689=CIRCLE('',#14756,0.274999999999999);
#5690=CIRCLE('',#14763,0.605);
#5691=CIRCLE('',#14764,0.605);
#5692=CIRCLE('',#14766,0.605);
#5693=CIRCLE('',#14768,0.605);
#6491=VERTEX_POINT('',#21322);
#6492=VERTEX_POINT('',#21324);
#6493=VERTEX_POINT('',#21328);
#6494=VERTEX_POINT('',#21330);
#6495=VERTEX_POINT('',#21334);
#6496=VERTEX_POINT('',#21336);
#6497=VERTEX_POINT('',#21340);
#6498=VERTEX_POINT('',#21342);
#6499=VERTEX_POINT('',#21346);
#6500=VERTEX_POINT('',#21348);
#6501=VERTEX_POINT('',#21352);
#6502=VERTEX_POINT('',#21354);
#6503=VERTEX_POINT('',#21358);
#6504=VERTEX_POINT('',#21360);
#6505=VERTEX_POINT('',#21364);
#6506=VERTEX_POINT('',#21366);
#6507=VERTEX_POINT('',#21370);
#6508=VERTEX_POINT('',#21372);
#6509=VERTEX_POINT('',#21376);
#6510=VERTEX_POINT('',#21377);
#6511=VERTEX_POINT('',#21379);
#6512=VERTEX_POINT('',#21381);
#6513=VERTEX_POINT('',#21385);
#6514=VERTEX_POINT('',#21386);
#6515=VERTEX_POINT('',#21388);
#6516=VERTEX_POINT('',#21390);
#6517=VERTEX_POINT('',#21394);
#6518=VERTEX_POINT('',#21395);
#6519=VERTEX_POINT('',#21400);
#6520=VERTEX_POINT('',#21401);
#6521=VERTEX_POINT('',#21406);
#6522=VERTEX_POINT('',#21408);
#6523=VERTEX_POINT('',#21413);
#6524=VERTEX_POINT('',#21416);
#6525=VERTEX_POINT('',#21418);
#6526=VERTEX_POINT('',#21421);
#6527=VERTEX_POINT('',#21425);
#6528=VERTEX_POINT('',#21429);
#7583=EDGE_CURVE('',#6491,#6491,#5672,.T.);
#7584=EDGE_CURVE('',#6491,#6492,#4218,.T.);
#7585=EDGE_CURVE('',#6492,#6492,#5673,.T.);
#7586=EDGE_CURVE('',#6493,#6493,#5674,.T.);
#7587=EDGE_CURVE('',#6493,#6494,#4219,.T.);
#7588=EDGE_CURVE('',#6494,#6494,#5675,.T.);
#7589=EDGE_CURVE('',#6495,#6495,#5676,.T.);
#7590=EDGE_CURVE('',#6495,#6496,#4220,.T.);
#7591=EDGE_CURVE('',#6496,#6496,#5677,.T.);
#7592=EDGE_CURVE('',#6497,#6497,#5678,.T.);
#7593=EDGE_CURVE('',#6497,#6498,#4221,.T.);
#7594=EDGE_CURVE('',#6498,#6498,#5679,.T.);
#7595=EDGE_CURVE('',#6499,#6499,#5680,.T.);
#7596=EDGE_CURVE('',#6499,#6500,#4222,.T.);
#7597=EDGE_CURVE('',#6500,#6500,#5681,.T.);
#7598=EDGE_CURVE('',#6501,#6501,#5682,.T.);
#7599=EDGE_CURVE('',#6501,#6502,#4223,.T.);
#7600=EDGE_CURVE('',#6502,#6502,#5683,.T.);
#7601=EDGE_CURVE('',#6503,#6503,#5684,.T.);
#7602=EDGE_CURVE('',#6503,#6504,#4224,.T.);
#7603=EDGE_CURVE('',#6504,#6504,#5685,.T.);
#7604=EDGE_CURVE('',#6505,#6505,#5686,.T.);
#7605=EDGE_CURVE('',#6505,#6506,#4225,.T.);
#7606=EDGE_CURVE('',#6506,#6506,#5687,.T.);
#7607=EDGE_CURVE('',#6507,#6507,#5688,.T.);
#7608=EDGE_CURVE('',#6507,#6508,#4226,.T.);
#7609=EDGE_CURVE('',#6508,#6508,#5689,.T.);
#7610=EDGE_CURVE('',#6509,#6510,#4227,.T.);
#7611=EDGE_CURVE('',#6509,#6511,#4228,.T.);
#7612=EDGE_CURVE('',#6511,#6512,#4229,.T.);
#7613=EDGE_CURVE('',#6512,#6510,#4230,.T.);
#7614=EDGE_CURVE('',#6513,#6514,#4231,.T.);
#7615=EDGE_CURVE('',#6513,#6515,#4232,.T.);
#7616=EDGE_CURVE('',#6515,#6516,#4233,.T.);
#7617=EDGE_CURVE('',#6516,#6514,#4234,.T.);
#7618=EDGE_CURVE('',#6517,#6518,#4235,.T.);
#7619=EDGE_CURVE('',#6518,#6516,#4236,.T.);
#7620=EDGE_CURVE('',#6517,#6515,#4237,.T.);
#7621=EDGE_CURVE('',#6519,#6520,#4238,.T.);
#7622=EDGE_CURVE('',#6520,#6512,#4239,.T.);
#7623=EDGE_CURVE('',#6519,#6511,#4240,.T.);
#7624=EDGE_CURVE('',#6509,#6521,#4241,.T.);
#7625=EDGE_CURVE('',#6522,#6521,#4242,.T.);
#7626=EDGE_CURVE('',#6514,#6522,#4243,.T.);
#7627=EDGE_CURVE('',#6518,#6519,#4244,.T.);
#7628=EDGE_CURVE('',#6510,#6523,#4245,.T.);
#7629=EDGE_CURVE('',#6521,#6523,#4246,.T.);
#7630=EDGE_CURVE('',#6524,#6524,#5690,.T.);
#7631=EDGE_CURVE('',#6525,#6525,#5691,.T.);
#7632=EDGE_CURVE('',#6524,#6526,#4247,.T.);
#7633=EDGE_CURVE('',#6526,#6526,#5692,.T.);
#7634=EDGE_CURVE('',#6525,#6527,#4248,.T.);
#7635=EDGE_CURVE('',#6527,#6527,#5693,.T.);
#7636=EDGE_CURVE('',#6528,#6522,#4249,.T.);
#7637=EDGE_CURVE('',#6513,#6528,#4250,.T.);
#7638=EDGE_CURVE('',#6523,#6528,#4251,.T.);
#7639=EDGE_CURVE('',#6520,#6517,#4252,.T.);
#9296=ORIENTED_EDGE('',*,*,#7583,.F.);
#9297=ORIENTED_EDGE('',*,*,#7584,.T.);
#9298=ORIENTED_EDGE('',*,*,#7585,.F.);
#9299=ORIENTED_EDGE('',*,*,#7584,.F.);
#9300=ORIENTED_EDGE('',*,*,#7586,.F.);
#9301=ORIENTED_EDGE('',*,*,#7587,.T.);
#9302=ORIENTED_EDGE('',*,*,#7588,.F.);
#9303=ORIENTED_EDGE('',*,*,#7587,.F.);
#9304=ORIENTED_EDGE('',*,*,#7589,.F.);
#9305=ORIENTED_EDGE('',*,*,#7590,.T.);
#9306=ORIENTED_EDGE('',*,*,#7591,.F.);
#9307=ORIENTED_EDGE('',*,*,#7590,.F.);
#9308=ORIENTED_EDGE('',*,*,#7592,.F.);
#9309=ORIENTED_EDGE('',*,*,#7593,.T.);
#9310=ORIENTED_EDGE('',*,*,#7594,.F.);
#9311=ORIENTED_EDGE('',*,*,#7593,.F.);
#9312=ORIENTED_EDGE('',*,*,#7595,.F.);
#9313=ORIENTED_EDGE('',*,*,#7596,.T.);
#9314=ORIENTED_EDGE('',*,*,#7597,.F.);
#9315=ORIENTED_EDGE('',*,*,#7596,.F.);
#9316=ORIENTED_EDGE('',*,*,#7598,.F.);
#9317=ORIENTED_EDGE('',*,*,#7599,.T.);
#9318=ORIENTED_EDGE('',*,*,#7600,.F.);
#9319=ORIENTED_EDGE('',*,*,#7599,.F.);
#9320=ORIENTED_EDGE('',*,*,#7601,.F.);
#9321=ORIENTED_EDGE('',*,*,#7602,.T.);
#9322=ORIENTED_EDGE('',*,*,#7603,.F.);
#9323=ORIENTED_EDGE('',*,*,#7602,.F.);
#9324=ORIENTED_EDGE('',*,*,#7604,.F.);
#9325=ORIENTED_EDGE('',*,*,#7605,.T.);
#9326=ORIENTED_EDGE('',*,*,#7606,.F.);
#9327=ORIENTED_EDGE('',*,*,#7605,.F.);
#9328=ORIENTED_EDGE('',*,*,#7607,.F.);
#9329=ORIENTED_EDGE('',*,*,#7608,.T.);
#9330=ORIENTED_EDGE('',*,*,#7609,.F.);
#9331=ORIENTED_EDGE('',*,*,#7608,.F.);
#9332=ORIENTED_EDGE('',*,*,#7610,.F.);
#9333=ORIENTED_EDGE('',*,*,#7611,.T.);
#9334=ORIENTED_EDGE('',*,*,#7612,.T.);
#9335=ORIENTED_EDGE('',*,*,#7613,.T.);
#9336=ORIENTED_EDGE('',*,*,#7603,.T.);
#9337=ORIENTED_EDGE('',*,*,#7606,.T.);
#9338=ORIENTED_EDGE('',*,*,#7614,.F.);
#9339=ORIENTED_EDGE('',*,*,#7615,.T.);
#9340=ORIENTED_EDGE('',*,*,#7616,.T.);
#9341=ORIENTED_EDGE('',*,*,#7617,.T.);
#9342=ORIENTED_EDGE('',*,*,#7600,.T.);
#9343=ORIENTED_EDGE('',*,*,#7609,.T.);
#9344=ORIENTED_EDGE('',*,*,#7618,.T.);
#9345=ORIENTED_EDGE('',*,*,#7619,.T.);
#9346=ORIENTED_EDGE('',*,*,#7616,.F.);
#9347=ORIENTED_EDGE('',*,*,#7620,.F.);
#9348=ORIENTED_EDGE('',*,*,#7621,.T.);
#9349=ORIENTED_EDGE('',*,*,#7622,.T.);
#9350=ORIENTED_EDGE('',*,*,#7612,.F.);
#9351=ORIENTED_EDGE('',*,*,#7623,.F.);
#9352=ORIENTED_EDGE('',*,*,#7624,.T.);
#9353=ORIENTED_EDGE('',*,*,#7625,.F.);
#9354=ORIENTED_EDGE('',*,*,#7626,.F.);
#9355=ORIENTED_EDGE('',*,*,#7617,.F.);
#9356=ORIENTED_EDGE('',*,*,#7619,.F.);
#9357=ORIENTED_EDGE('',*,*,#7627,.T.);
#9358=ORIENTED_EDGE('',*,*,#7623,.T.);
#9359=ORIENTED_EDGE('',*,*,#7611,.F.);
#9360=ORIENTED_EDGE('',*,*,#7610,.T.);
#9361=ORIENTED_EDGE('',*,*,#7628,.T.);
#9362=ORIENTED_EDGE('',*,*,#7629,.F.);
#9363=ORIENTED_EDGE('',*,*,#7624,.F.);
#9364=ORIENTED_EDGE('',*,*,#7630,.T.);
#9365=ORIENTED_EDGE('',*,*,#7631,.T.);
#9366=ORIENTED_EDGE('',*,*,#7595,.T.);
#9367=ORIENTED_EDGE('',*,*,#7592,.T.);
#9368=ORIENTED_EDGE('',*,*,#7589,.T.);
#9369=ORIENTED_EDGE('',*,*,#7586,.T.);
#9370=ORIENTED_EDGE('',*,*,#7583,.T.);
#9371=ORIENTED_EDGE('',*,*,#7630,.F.);
#9372=ORIENTED_EDGE('',*,*,#7632,.T.);
#9373=ORIENTED_EDGE('',*,*,#7633,.F.);
#9374=ORIENTED_EDGE('',*,*,#7632,.F.);
#9375=ORIENTED_EDGE('',*,*,#7631,.F.);
#9376=ORIENTED_EDGE('',*,*,#7634,.T.);
#9377=ORIENTED_EDGE('',*,*,#7635,.F.);
#9378=ORIENTED_EDGE('',*,*,#7634,.F.);
#9379=ORIENTED_EDGE('',*,*,#7614,.T.);
#9380=ORIENTED_EDGE('',*,*,#7626,.T.);
#9381=ORIENTED_EDGE('',*,*,#7636,.F.);
#9382=ORIENTED_EDGE('',*,*,#7637,.F.);
#9383=ORIENTED_EDGE('',*,*,#7635,.T.);
#9384=ORIENTED_EDGE('',*,*,#7633,.T.);
#9385=ORIENTED_EDGE('',*,*,#7597,.T.);
#9386=ORIENTED_EDGE('',*,*,#7594,.T.);
#9387=ORIENTED_EDGE('',*,*,#7591,.T.);
#9388=ORIENTED_EDGE('',*,*,#7588,.T.);
#9389=ORIENTED_EDGE('',*,*,#7585,.T.);
#9390=ORIENTED_EDGE('',*,*,#7637,.T.);
#9391=ORIENTED_EDGE('',*,*,#7638,.F.);
#9392=ORIENTED_EDGE('',*,*,#7628,.F.);
#9393=ORIENTED_EDGE('',*,*,#7613,.F.);
#9394=ORIENTED_EDGE('',*,*,#7622,.F.);
#9395=ORIENTED_EDGE('',*,*,#7639,.T.);
#9396=ORIENTED_EDGE('',*,*,#7620,.T.);
#9397=ORIENTED_EDGE('',*,*,#7615,.F.);
#9398=ORIENTED_EDGE('',*,*,#7629,.T.);
#9399=ORIENTED_EDGE('',*,*,#7638,.T.);
#9400=ORIENTED_EDGE('',*,*,#7636,.T.);
#9401=ORIENTED_EDGE('',*,*,#7625,.T.);
#9402=ORIENTED_EDGE('',*,*,#7627,.F.);
#9403=ORIENTED_EDGE('',*,*,#7618,.F.);
#9404=ORIENTED_EDGE('',*,*,#7639,.F.);
#9405=ORIENTED_EDGE('',*,*,#7621,.F.);
#9406=ORIENTED_EDGE('',*,*,#7598,.T.);
#9407=ORIENTED_EDGE('',*,*,#7601,.T.);
#9408=ORIENTED_EDGE('',*,*,#7604,.T.);
#9409=ORIENTED_EDGE('',*,*,#7607,.T.);
#12108=CYLINDRICAL_SURFACE('',#14730,0.165);
#12109=CYLINDRICAL_SURFACE('',#14733,0.165);
#12110=CYLINDRICAL_SURFACE('',#14736,0.165);
#12111=CYLINDRICAL_SURFACE('',#14739,0.165);
#12112=CYLINDRICAL_SURFACE('',#14742,1.6);
#12113=CYLINDRICAL_SURFACE('',#14745,0.274999999999999);
#12114=CYLINDRICAL_SURFACE('',#14748,0.274999999999999);
#12115=CYLINDRICAL_SURFACE('',#14751,0.274999999999999);
#12116=CYLINDRICAL_SURFACE('',#14754,0.274999999999999);
#12117=CYLINDRICAL_SURFACE('',#14765,0.605);
#12118=CYLINDRICAL_SURFACE('',#14767,0.605);
#12498=ADVANCED_FACE('',(#2131),#12108,.F.);
#12499=ADVANCED_FACE('',(#2132),#12109,.F.);
#12500=ADVANCED_FACE('',(#2133),#12110,.F.);
#12501=ADVANCED_FACE('',(#2134),#12111,.F.);
#12502=ADVANCED_FACE('',(#2135),#12112,.F.);
#12503=ADVANCED_FACE('',(#2136),#12113,.F.);
#12504=ADVANCED_FACE('',(#2137),#12114,.F.);
#12505=ADVANCED_FACE('',(#2138),#12115,.F.);
#12506=ADVANCED_FACE('',(#2139),#12116,.F.);
#12507=ADVANCED_FACE('',(#2140,#1277,#1278),#1674,.T.);
#12508=ADVANCED_FACE('',(#2141,#1279,#1280),#1675,.T.);
#12509=ADVANCED_FACE('',(#2142),#1676,.T.);
#12510=ADVANCED_FACE('',(#2143),#1677,.T.);
#12511=ADVANCED_FACE('',(#2144),#1678,.T.);
#12512=ADVANCED_FACE('',(#2145,#1281,#1282,#1283,#1284,#1285,#1286,#1287),
#1679,.T.);
#12513=ADVANCED_FACE('',(#2146),#12117,.F.);
#12514=ADVANCED_FACE('',(#2147),#12118,.F.);
#12515=ADVANCED_FACE('',(#2148,#1288,#1289,#1290,#1291,#1292,#1293,#1294),
#1680,.T.);
#12516=ADVANCED_FACE('',(#2149),#1681,.T.);
#12517=ADVANCED_FACE('',(#2150),#1682,.T.);
#12518=ADVANCED_FACE('',(#2151,#1295,#1296,#1297,#1298),#1683,.F.);
#13254=CLOSED_SHELL('',(#12498,#12499,#12500,#12501,#12502,#12503,#12504,
#12505,#12506,#12507,#12508,#12509,#12510,#12511,#12512,#12513,#12514,#12515,
#12516,#12517,#12518));
#14729=AXIS2_PLACEMENT_3D('',#21320,#16850,#16851);
#14730=AXIS2_PLACEMENT_3D('',#21321,#16852,#16853);
#14731=AXIS2_PLACEMENT_3D('',#21323,#16854,#16855);
#14732=AXIS2_PLACEMENT_3D('',#21326,#16857,#16858);
#14733=AXIS2_PLACEMENT_3D('',#21327,#16859,#16860);
#14734=AXIS2_PLACEMENT_3D('',#21329,#16861,#16862);
#14735=AXIS2_PLACEMENT_3D('',#21332,#16864,#16865);
#14736=AXIS2_PLACEMENT_3D('',#21333,#16866,#16867);
#14737=AXIS2_PLACEMENT_3D('',#21335,#16868,#16869);
#14738=AXIS2_PLACEMENT_3D('',#21338,#16871,#16872);
#14739=AXIS2_PLACEMENT_3D('',#21339,#16873,#16874);
#14740=AXIS2_PLACEMENT_3D('',#21341,#16875,#16876);
#14741=AXIS2_PLACEMENT_3D('',#21344,#16878,#16879);
#14742=AXIS2_PLACEMENT_3D('',#21345,#16880,#16881);
#14743=AXIS2_PLACEMENT_3D('',#21347,#16882,#16883);
#14744=AXIS2_PLACEMENT_3D('',#21350,#16885,#16886);
#14745=AXIS2_PLACEMENT_3D('',#21351,#16887,#16888);
#14746=AXIS2_PLACEMENT_3D('',#21353,#16889,#16890);
#14747=AXIS2_PLACEMENT_3D('',#21356,#16892,#16893);
#14748=AXIS2_PLACEMENT_3D('',#21357,#16894,#16895);
#14749=AXIS2_PLACEMENT_3D('',#21359,#16896,#16897);
#14750=AXIS2_PLACEMENT_3D('',#21362,#16899,#16900);
#14751=AXIS2_PLACEMENT_3D('',#21363,#16901,#16902);
#14752=AXIS2_PLACEMENT_3D('',#21365,#16903,#16904);
#14753=AXIS2_PLACEMENT_3D('',#21368,#16906,#16907);
#14754=AXIS2_PLACEMENT_3D('',#21369,#16908,#16909);
#14755=AXIS2_PLACEMENT_3D('',#21371,#16910,#16911);
#14756=AXIS2_PLACEMENT_3D('',#21374,#16913,#16914);
#14757=AXIS2_PLACEMENT_3D('',#21375,#16915,#16916);
#14758=AXIS2_PLACEMENT_3D('',#21384,#16921,#16922);
#14759=AXIS2_PLACEMENT_3D('',#21393,#16927,#16928);
#14760=AXIS2_PLACEMENT_3D('',#21399,#16932,#16933);
#14761=AXIS2_PLACEMENT_3D('',#21405,#16937,#16938);
#14762=AXIS2_PLACEMENT_3D('',#21412,#16943,#16944);
#14763=AXIS2_PLACEMENT_3D('',#21417,#16947,#16948);
#14764=AXIS2_PLACEMENT_3D('',#21419,#16949,#16950);
#14765=AXIS2_PLACEMENT_3D('',#21420,#16951,#16952);
#14766=AXIS2_PLACEMENT_3D('',#21423,#16954,#16955);
#14767=AXIS2_PLACEMENT_3D('',#21424,#16956,#16957);
#14768=AXIS2_PLACEMENT_3D('',#21427,#16959,#16960);
#14769=AXIS2_PLACEMENT_3D('',#21428,#16961,#16962);
#14770=AXIS2_PLACEMENT_3D('',#21432,#16965,#16966);
#14771=AXIS2_PLACEMENT_3D('',#21435,#16969,#16970);
#14772=AXIS2_PLACEMENT_3D('',#21436,#16971,#16972);
#16850=DIRECTION('axis',(0.,0.,1.));
#16851=DIRECTION('refdir',(1.,0.,0.));
#16852=DIRECTION('center_axis',(1.,0.,0.));
#16853=DIRECTION('ref_axis',(0.,0.,-1.));
#16854=DIRECTION('center_axis',(1.,0.,0.));
#16855=DIRECTION('ref_axis',(0.,0.,-1.));
#16856=DIRECTION('',(1.,0.,0.));
#16857=DIRECTION('center_axis',(-1.,0.,0.));
#16858=DIRECTION('ref_axis',(0.,0.,-1.));
#16859=DIRECTION('center_axis',(1.,0.,0.));
#16860=DIRECTION('ref_axis',(0.,0.,-1.));
#16861=DIRECTION('center_axis',(1.,0.,0.));
#16862=DIRECTION('ref_axis',(0.,0.,-1.));
#16863=DIRECTION('',(1.,0.,0.));
#16864=DIRECTION('center_axis',(-1.,0.,0.));
#16865=DIRECTION('ref_axis',(0.,0.,-1.));
#16866=DIRECTION('center_axis',(1.,0.,0.));
#16867=DIRECTION('ref_axis',(0.,0.,-1.));
#16868=DIRECTION('center_axis',(1.,0.,0.));
#16869=DIRECTION('ref_axis',(0.,0.,-1.));
#16870=DIRECTION('',(1.,0.,0.));
#16871=DIRECTION('center_axis',(-1.,0.,0.));
#16872=DIRECTION('ref_axis',(0.,0.,-1.));
#16873=DIRECTION('center_axis',(1.,0.,0.));
#16874=DIRECTION('ref_axis',(0.,0.,-1.));
#16875=DIRECTION('center_axis',(1.,0.,0.));
#16876=DIRECTION('ref_axis',(0.,0.,-1.));
#16877=DIRECTION('',(1.,0.,0.));
#16878=DIRECTION('center_axis',(-1.,0.,0.));
#16879=DIRECTION('ref_axis',(0.,0.,-1.));
#16880=DIRECTION('center_axis',(1.,0.,0.));
#16881=DIRECTION('ref_axis',(0.,0.,-1.));
#16882=DIRECTION('center_axis',(1.,0.,0.));
#16883=DIRECTION('ref_axis',(0.,0.,-1.));
#16884=DIRECTION('',(1.,0.,0.));
#16885=DIRECTION('center_axis',(-1.,0.,0.));
#16886=DIRECTION('ref_axis',(0.,0.,-1.));
#16887=DIRECTION('center_axis',(0.,0.,1.));
#16888=DIRECTION('ref_axis',(1.,0.,0.));
#16889=DIRECTION('center_axis',(0.,0.,1.));
#16890=DIRECTION('ref_axis',(1.,0.,0.));
#16891=DIRECTION('',(0.,0.,1.));
#16892=DIRECTION('center_axis',(0.,0.,-1.));
#16893=DIRECTION('ref_axis',(1.,0.,0.));
#16894=DIRECTION('center_axis',(0.,0.,1.));
#16895=DIRECTION('ref_axis',(1.,0.,0.));
#16896=DIRECTION('center_axis',(0.,0.,1.));
#16897=DIRECTION('ref_axis',(1.,0.,0.));
#16898=DIRECTION('',(0.,0.,1.));
#16899=DIRECTION('center_axis',(0.,0.,-1.));
#16900=DIRECTION('ref_axis',(1.,0.,0.));
#16901=DIRECTION('center_axis',(0.,0.,1.));
#16902=DIRECTION('ref_axis',(1.,0.,0.));
#16903=DIRECTION('center_axis',(0.,0.,1.));
#16904=DIRECTION('ref_axis',(1.,0.,0.));
#16905=DIRECTION('',(0.,0.,1.));
#16906=DIRECTION('center_axis',(0.,0.,-1.));
#16907=DIRECTION('ref_axis',(1.,0.,0.));
#16908=DIRECTION('center_axis',(0.,0.,1.));
#16909=DIRECTION('ref_axis',(1.,0.,0.));
#16910=DIRECTION('center_axis',(0.,0.,1.));
#16911=DIRECTION('ref_axis',(1.,0.,0.));
#16912=DIRECTION('',(0.,0.,1.));
#16913=DIRECTION('center_axis',(0.,0.,-1.));
#16914=DIRECTION('ref_axis',(1.,0.,0.));
#16915=DIRECTION('center_axis',(0.,0.,1.));
#16916=DIRECTION('ref_axis',(1.,0.,0.));
#16917=DIRECTION('',(0.,-1.,0.));
#16918=DIRECTION('',(-1.,0.,0.));
#16919=DIRECTION('',(0.,-1.,0.));
#16920=DIRECTION('',(1.,0.,0.));
#16921=DIRECTION('center_axis',(0.,0.,1.));
#16922=DIRECTION('ref_axis',(1.,0.,0.));
#16923=DIRECTION('',(0.,1.,0.));
#16924=DIRECTION('',(1.,0.,0.));
#16925=DIRECTION('',(0.,1.,0.));
#16926=DIRECTION('',(-1.,0.,0.));
#16927=DIRECTION('center_axis',(1.,0.,0.));
#16928=DIRECTION('ref_axis',(0.,1.,0.));
#16929=DIRECTION('',(0.,1.,0.));
#16930=DIRECTION('',(0.,0.,1.));
#16931=DIRECTION('',(0.,0.,1.));
#16932=DIRECTION('center_axis',(-1.,0.,0.));
#16933=DIRECTION('ref_axis',(0.,-1.,0.));
#16934=DIRECTION('',(0.,-1.,0.));
#16935=DIRECTION('',(0.,0.,1.));
#16936=DIRECTION('',(0.,0.,1.));
#16937=DIRECTION('center_axis',(0.,1.,0.));
#16938=DIRECTION('ref_axis',(-1.,0.,0.));
#16939=DIRECTION('',(0.,0.,1.));
#16940=DIRECTION('',(-1.,0.,0.));
#16941=DIRECTION('',(0.,0.,1.));
#16942=DIRECTION('',(-1.,0.,0.));
#16943=DIRECTION('center_axis',(-1.,0.,0.));
#16944=DIRECTION('ref_axis',(0.,-1.,0.));
#16945=DIRECTION('',(0.,0.,1.));
#16946=DIRECTION('',(0.,-1.,0.));
#16947=DIRECTION('center_axis',(1.,0.,0.));
#16948=DIRECTION('ref_axis',(0.,0.,-1.));
#16949=DIRECTION('center_axis',(1.,0.,0.));
#16950=DIRECTION('ref_axis',(0.,0.,-1.));
#16951=DIRECTION('center_axis',(1.,0.,0.));
#16952=DIRECTION('ref_axis',(0.,0.,-1.));
#16953=DIRECTION('',(1.,0.,0.));
#16954=DIRECTION('center_axis',(-1.,0.,0.));
#16955=DIRECTION('ref_axis',(0.,0.,-1.));
#16956=DIRECTION('center_axis',(1.,0.,0.));
#16957=DIRECTION('ref_axis',(0.,0.,-1.));
#16958=DIRECTION('',(1.,0.,0.));
#16959=DIRECTION('center_axis',(-1.,0.,0.));
#16960=DIRECTION('ref_axis',(0.,0.,-1.));
#16961=DIRECTION('center_axis',(1.,0.,0.));
#16962=DIRECTION('ref_axis',(0.,1.,0.));
#16963=DIRECTION('',(0.,1.,0.));
#16964=DIRECTION('',(0.,0.,1.));
#16965=DIRECTION('center_axis',(0.,-1.,0.));
#16966=DIRECTION('ref_axis',(1.,0.,0.));
#16967=DIRECTION('',(1.,0.,0.));
#16968=DIRECTION('',(1.,0.,0.));
#16969=DIRECTION('center_axis',(0.,0.,1.));
#16970=DIRECTION('ref_axis',(1.,0.,0.));
#16971=DIRECTION('center_axis',(0.,0.,1.));
#16972=DIRECTION('ref_axis',(1.,0.,0.));
#21320=CARTESIAN_POINT('',(0.,0.,0.));
#21321=CARTESIAN_POINT('Origin',(43.9,-1.30814754519511,4.69185245480489));
#21322=CARTESIAN_POINT('',(44.,-1.30814754519511,4.85685245480489));
#21323=CARTESIAN_POINT('Origin',(44.,-1.30814754519511,4.69185245480489));
#21324=CARTESIAN_POINT('',(46.,-1.30814754519511,4.85685245480489));
#21325=CARTESIAN_POINT('',(43.9,-1.30814754519511,4.85685245480489));
#21326=CARTESIAN_POINT('Origin',(46.,-1.30814754519511,4.69185245480489));
#21327=CARTESIAN_POINT('Origin',(43.9,-1.30814754519511,7.30814754519511));
#21328=CARTESIAN_POINT('',(44.,-1.30814754519511,7.47314754519511));
#21329=CARTESIAN_POINT('Origin',(44.,-1.30814754519511,7.30814754519511));
#21330=CARTESIAN_POINT('',(46.,-1.30814754519511,7.47314754519511));
#21331=CARTESIAN_POINT('',(43.9,-1.30814754519511,7.47314754519511));
#21332=CARTESIAN_POINT('Origin',(46.,-1.30814754519511,7.30814754519511));
#21333=CARTESIAN_POINT('Origin',(43.9,1.30814754519511,7.30814754519511));
#21334=CARTESIAN_POINT('',(44.,1.30814754519511,7.47314754519511));
#21335=CARTESIAN_POINT('Origin',(44.,1.30814754519511,7.30814754519511));
#21336=CARTESIAN_POINT('',(46.,1.30814754519511,7.47314754519511));
#21337=CARTESIAN_POINT('',(43.9,1.30814754519511,7.47314754519511));
#21338=CARTESIAN_POINT('Origin',(46.,1.30814754519511,7.30814754519511));
#21339=CARTESIAN_POINT('Origin',(43.9,1.30814754519511,4.69185245480489));
#21340=CARTESIAN_POINT('',(44.,1.30814754519511,4.85685245480489));
#21341=CARTESIAN_POINT('Origin',(44.,1.30814754519511,4.69185245480489));
#21342=CARTESIAN_POINT('',(46.,1.30814754519511,4.85685245480489));
#21343=CARTESIAN_POINT('',(43.9,1.30814754519511,4.85685245480489));
#21344=CARTESIAN_POINT('Origin',(46.,1.30814754519511,4.69185245480489));
#21345=CARTESIAN_POINT('Origin',(43.9,0.,6.));
#21346=CARTESIAN_POINT('',(44.,-1.95943487863576E-16,7.6));
#21347=CARTESIAN_POINT('Origin',(44.,0.,6.));
#21348=CARTESIAN_POINT('',(46.,1.95943487863576E-16,7.6));
#21349=CARTESIAN_POINT('',(43.9,-1.95943487863576E-16,7.6));
#21350=CARTESIAN_POINT('Origin',(46.,0.,6.));
#21351=CARTESIAN_POINT('Origin',(46.5,-4.,0.9));
#21352=CARTESIAN_POINT('',(46.225,-4.,1.));
#21353=CARTESIAN_POINT('Origin',(46.5,-4.,1.));
#21354=CARTESIAN_POINT('',(46.225,-4.,2.));
#21355=CARTESIAN_POINT('',(46.225,-4.,0.9));
#21356=CARTESIAN_POINT('Origin',(46.5,-4.,2.));
#21357=CARTESIAN_POINT('Origin',(43.5,4.,0.9));
#21358=CARTESIAN_POINT('',(43.225,4.,1.));
#21359=CARTESIAN_POINT('Origin',(43.5,4.,1.));
#21360=CARTESIAN_POINT('',(43.225,4.,2.));
#21361=CARTESIAN_POINT('',(43.225,4.,0.9));
#21362=CARTESIAN_POINT('Origin',(43.5,4.,2.));
#21363=CARTESIAN_POINT('Origin',(43.5,-4.,0.9));
#21364=CARTESIAN_POINT('',(43.225,-4.,1.));
#21365=CARTESIAN_POINT('Origin',(43.5,-4.,1.));
#21366=CARTESIAN_POINT('',(43.225,-4.,2.));
#21367=CARTESIAN_POINT('',(43.225,-4.,0.9));
#21368=CARTESIAN_POINT('Origin',(43.5,-4.,2.));
#21369=CARTESIAN_POINT('Origin',(46.5,4.,0.9));
#21370=CARTESIAN_POINT('',(46.225,4.,1.));
#21371=CARTESIAN_POINT('Origin',(46.5,4.,1.));
#21372=CARTESIAN_POINT('',(46.225,4.,2.));
#21373=CARTESIAN_POINT('',(46.225,4.,0.9));
#21374=CARTESIAN_POINT('Origin',(46.5,4.,2.));
#21375=CARTESIAN_POINT('Origin',(45.,0.,2.));
#21376=CARTESIAN_POINT('',(44.,5.,2.));
#21377=CARTESIAN_POINT('',(44.,-5.,2.));
#21378=CARTESIAN_POINT('',(44.,2.5,2.));
#21379=CARTESIAN_POINT('',(43.,5.,2.));
#21380=CARTESIAN_POINT('',(47.,5.,2.));
#21381=CARTESIAN_POINT('',(43.,-5.,2.));
#21382=CARTESIAN_POINT('',(43.,5.,2.));
#21383=CARTESIAN_POINT('',(43.,-5.,2.));
#21384=CARTESIAN_POINT('Origin',(45.,0.,2.));
#21385=CARTESIAN_POINT('',(46.,-5.,2.));
#21386=CARTESIAN_POINT('',(46.,5.,2.));
#21387=CARTESIAN_POINT('',(46.,-2.5,2.));
#21388=CARTESIAN_POINT('',(47.,-5.,2.));
#21389=CARTESIAN_POINT('',(43.,-5.,2.));
#21390=CARTESIAN_POINT('',(47.,5.,2.));
#21391=CARTESIAN_POINT('',(47.,-5.,2.));
#21392=CARTESIAN_POINT('',(47.,5.,2.));
#21393=CARTESIAN_POINT('Origin',(47.,-5.,1.));
#21394=CARTESIAN_POINT('',(47.,-5.,1.));
#21395=CARTESIAN_POINT('',(47.,5.,1.));
#21396=CARTESIAN_POINT('',(47.,-5.,1.));
#21397=CARTESIAN_POINT('',(47.,5.,1.));
#21398=CARTESIAN_POINT('',(47.,-5.,1.));
#21399=CARTESIAN_POINT('Origin',(43.,5.,1.));
#21400=CARTESIAN_POINT('',(43.,5.,1.));
#21401=CARTESIAN_POINT('',(43.,-5.,1.));
#21402=CARTESIAN_POINT('',(43.,5.,1.));
#21403=CARTESIAN_POINT('',(43.,-5.,1.));
#21404=CARTESIAN_POINT('',(43.,5.,1.));
#21405=CARTESIAN_POINT('Origin',(46.,5.,1.));
#21406=CARTESIAN_POINT('',(44.,5.,8.5));
#21407=CARTESIAN_POINT('',(44.,5.,1.));
#21408=CARTESIAN_POINT('',(46.,5.,8.5));
#21409=CARTESIAN_POINT('',(46.,5.,8.5));
#21410=CARTESIAN_POINT('',(46.,5.,1.));
#21411=CARTESIAN_POINT('',(47.,5.,1.));
#21412=CARTESIAN_POINT('Origin',(44.,5.,1.));
#21413=CARTESIAN_POINT('',(44.,-5.,8.5));
#21414=CARTESIAN_POINT('',(44.,-5.,1.));
#21415=CARTESIAN_POINT('',(44.,5.,8.5));
#21416=CARTESIAN_POINT('',(44.,-3.,6.605));
#21417=CARTESIAN_POINT('Origin',(44.,-3.,6.));
#21418=CARTESIAN_POINT('',(44.,3.,6.605));
#21419=CARTESIAN_POINT('Origin',(44.,3.,6.));
#21420=CARTESIAN_POINT('Origin',(43.9,-3.,6.));
#21421=CARTESIAN_POINT('',(46.,-3.,6.605));
#21422=CARTESIAN_POINT('',(43.9,-3.,6.605));
#21423=CARTESIAN_POINT('Origin',(46.,-3.,6.));
#21424=CARTESIAN_POINT('Origin',(43.9,3.,6.));
#21425=CARTESIAN_POINT('',(46.,3.,6.605));
#21426=CARTESIAN_POINT('',(43.9,3.,6.605));
#21427=CARTESIAN_POINT('Origin',(46.,3.,6.));
#21428=CARTESIAN_POINT('Origin',(46.,-5.,1.));
#21429=CARTESIAN_POINT('',(46.,-5.,8.5));
#21430=CARTESIAN_POINT('',(46.,-5.,8.5));
#21431=CARTESIAN_POINT('',(46.,-5.,1.));
#21432=CARTESIAN_POINT('Origin',(44.,-5.,1.));
#21433=CARTESIAN_POINT('',(44.,-5.,8.5));
#21434=CARTESIAN_POINT('',(43.,-5.,1.));
#21435=CARTESIAN_POINT('Origin',(45.,0.,8.5));
#21436=CARTESIAN_POINT('Origin',(45.,0.,1.));
#24867=UNCERTAINTY_MEASURE_WITH_UNIT(LENGTH_MEASURE(0.001),#25101,
'DISTANCE_ACCURACY_VALUE',
'Maximum model space distance between geometric entities at asserted c
onnectivities');
#24979=UNCERTAINTY_MEASURE_WITH_UNIT(LENGTH_MEASURE(0.001),#25101,
'DISTANCE_ACCURACY_VALUE',
'Maximum model space distance between geometric entities at asserted c
onnectivities');
#24988=(
GEOMETRIC_REPRESENTATION_CONTEXT(3)
GLOBAL_UNCERTAINTY_ASSIGNED_CONTEXT((#24867))
GLOBAL_UNIT_ASSIGNED_CONTEXT((#25101,#25103,#25104))
REPRESENTATION_CONTEXT('','3D')
);
#25100=(
GEOMETRIC_REPRESENTATION_CONTEXT(3)
GLOBAL_UNCERTAINTY_ASSIGNED_CONTEXT((#24979))
GLOBAL_UNIT_ASSIGNED_CONTEXT((#25101,#25103,#25104))
REPRESENTATION_CONTEXT('','3D')
);
#25101=(
LENGTH_UNIT()
NAMED_UNIT(*)
SI_UNIT(.CENTI.,.METRE.)
);
#25103=(
NAMED_UNIT(*)
PLANE_ANGLE_UNIT()
SI_UNIT($,.RADIAN.)
);
#25104=(
NAMED_UNIT(*)
SI_UNIT($,.STERADIAN.)
SOLID_ANGLE_UNIT()
);
#25113=SHAPE_DEFINITION_REPRESENTATION(#25233,#25518);
#25233=PRODUCT_DEFINITION_SHAPE('',$,#25639);
#25518=SHAPE_REPRESENTATION('',(#14729),#24988);
#25630=PRODUCT_DEFINITION_CONTEXT('part definition',#25992,'design');
#25639=PRODUCT_DEFINITION('Lower screw support','Lower screw support',#25759,
#25630);
#25759=PRODUCT_DEFINITION_FORMATION('',$,#26002);
#25992=APPLICATION_CONTEXT(
'Core Data for Automotive Mechanical Design Process');
#25993=PRODUCT_CONTEXT('part definition',#25992,'mechanical');
#26002=PRODUCT('Lower screw support','Lower screw support',
'Lower screw support',(#25993));
#26192=COLOUR_RGB('Black',0.12,0.14,0.17);
#26193=FILL_AREA_STYLE_COLOUR('',#26192);
#26194=FILL_AREA_STYLE('',(#26193));
#26195=SURFACE_STYLE_FILL_AREA(#26194);
#26196=SURFACE_SIDE_STYLE('',(#26195));
#26197=SURFACE_STYLE_USAGE(.BOTH.,#26196);
#26198=PRESENTATION_STYLE_ASSIGNMENT((#26197));
ENDSEC;
END-ISO-10303-21;
